ISO-10303-21;
HEADER;
/* Generated by software containing ST-Developer
 * from STEP Tools, Inc. (www.steptools.com) 
 */

FILE_DESCRIPTION(
/* description */ ('Bell-crank linkage with push rods'),
/* implementation_level */ '2;1');

FILE_NAME(
/* name */ 'Vertical link pin (1).step',
/* time_stamp */ '2026-10-28T03:25:15-07:00',
/* author */ (''),
/* organization */ (''),
/* preprocessor_version */ 'ST-DEVELOPER v20.2',
/* originating_system */ 'Autodesk Translation Framework v15.17.0.0',
/* authorisation */ '');

FILE_SCHEMA (('AUTOMOTIVE_DESIGN { 1 0 10303 214 3 1 1 }'));
ENDSEC;

DATA;
#10=MECHANICAL_DESIGN_GEOMETRIC_PRESENTATION_REPRESENTATION('',(#659),#16678);
#543=SHAPE_REPRESENTATION_RELATIONSHIP('SRR','None',#16965,#597);
#597=ADVANCED_BREP_SHAPE_REPRESENTATION('',(#719),#16670);
#659=STYLED_ITEM('',(#17291),#719);
#719=MANIFOLD_SOLID_BREP('Body1',#8851);
#945=FACE_BOUND('',#2452,.T.);
#946=FACE_BOUND('',#2454,.T.);
#947=FACE_BOUND('',#2459,.T.);
#1208=PLANE('',#10425);
#1209=PLANE('',#10426);
#1210=PLANE('',#10429);
#1211=PLANE('',#10437);
#1212=PLANE('',#10438);
#1707=FACE_OUTER_BOUND('',#2449,.T.);
#1708=FACE_OUTER_BOUND('',#2450,.T.);
#1709=FACE_OUTER_BOUND('',#2451,.T.);
#1710=FACE_OUTER_BOUND('',#2453,.T.);
#1711=FACE_OUTER_BOUND('',#2455,.T.);
#1712=FACE_OUTER_BOUND('',#2456,.T.);
#1713=FACE_OUTER_BOUND('',#2457,.T.);
#1714=FACE_OUTER_BOUND('',#2458,.T.);
#1715=FACE_OUTER_BOUND('',#2460,.T.);
#2449=EDGE_LOOP('',(#7851,#7852,#7853,#7854));
#2450=EDGE_LOOP('',(#7855));
#2451=EDGE_LOOP('',(#7856));
#2452=EDGE_LOOP('',(#7857));
#2453=EDGE_LOOP('',(#7858));
#2454=EDGE_LOOP('',(#7859));
#2455=EDGE_LOOP('',(#7860,#7861,#7862,#7863));
#2456=EDGE_LOOP('',(#7864,#7865,#7866,#7867));
#2457=EDGE_LOOP('',(#7868,#7869,#7870,#7871));
#2458=EDGE_LOOP('',(#7872));
#2459=EDGE_LOOP('',(#7873));
#2460=EDGE_LOOP('',(#7874));
#3022=LINE('',#16217,#3571);
#3023=LINE('',#16231,#3572);
#3024=LINE('',#16234,#3573);
#3025=LINE('',#16239,#3574);
#3571=VECTOR('',#13060,0.165);
#3572=VECTOR('',#13079,0.7);
#3573=VECTOR('',#13082,0.3);
#3574=VECTOR('',#13089,0.3);
#4071=CIRCLE('',#10423,0.165);
#4072=CIRCLE('',#10424,0.165);
#4073=CIRCLE('',#10427,0.7);
#4074=CIRCLE('',#10428,0.3);
#4075=CIRCLE('',#10430,0.7);
#4076=CIRCLE('',#10431,0.3);
#4077=CIRCLE('',#10434,0.3);
#4078=CIRCLE('',#10436,0.3);
#4762=VERTEX_POINT('',#16214);
#4763=VERTEX_POINT('',#16216);
#4764=VERTEX_POINT('',#16221);
#4765=VERTEX_POINT('',#16223);
#4766=VERTEX_POINT('',#16226);
#4767=VERTEX_POINT('',#16228);
#4768=VERTEX_POINT('',#16233);
#4769=VERTEX_POINT('',#16237);
#5803=EDGE_CURVE('',#4762,#4762,#4071,.T.);
#5804=EDGE_CURVE('',#4762,#4763,#3022,.T.);
#5805=EDGE_CURVE('',#4763,#4763,#4072,.T.);
#5806=EDGE_CURVE('',#4764,#4764,#4073,.T.);
#5807=EDGE_CURVE('',#4765,#4765,#4074,.T.);
#5808=EDGE_CURVE('',#4766,#4766,#4075,.T.);
#5809=EDGE_CURVE('',#4767,#4767,#4076,.T.);
#5810=EDGE_CURVE('',#4764,#4766,#3023,.T.);
#5811=EDGE_CURVE('',#4767,#4768,#3024,.T.);
#5812=EDGE_CURVE('',#4768,#4768,#4077,.T.);
#5813=EDGE_CURVE('',#4769,#4769,#4078,.T.);
#5814=EDGE_CURVE('',#4769,#4765,#3025,.T.);
#7851=ORIENTED_EDGE('',*,*,#5803,.F.);
#7852=ORIENTED_EDGE('',*,*,#5804,.T.);
#7853=ORIENTED_EDGE('',*,*,#5805,.F.);
#7854=ORIENTED_EDGE('',*,*,#5804,.F.);
#7855=ORIENTED_EDGE('',*,*,#5803,.T.);
#7856=ORIENTED_EDGE('',*,*,#5806,.T.);
#7857=ORIENTED_EDGE('',*,*,#5807,.F.);
#7858=ORIENTED_EDGE('',*,*,#5808,.F.);
#7859=ORIENTED_EDGE('',*,*,#5809,.F.);
#7860=ORIENTED_EDGE('',*,*,#5806,.F.);
#7861=ORIENTED_EDGE('',*,*,#5810,.T.);
#7862=ORIENTED_EDGE('',*,*,#5808,.T.);
#7863=ORIENTED_EDGE('',*,*,#5810,.F.);
#7864=ORIENTED_EDGE('',*,*,#5809,.T.);
#7865=ORIENTED_EDGE('',*,*,#5811,.T.);
#7866=ORIENTED_EDGE('',*,*,#5812,.T.);
#7867=ORIENTED_EDGE('',*,*,#5811,.F.);
#7868=ORIENTED_EDGE('',*,*,#5813,.F.);
#7869=ORIENTED_EDGE('',*,*,#5814,.T.);
#7870=ORIENTED_EDGE('',*,*,#5807,.T.);
#7871=ORIENTED_EDGE('',*,*,#5814,.F.);
#7872=ORIENTED_EDGE('',*,*,#5813,.T.);
#7873=ORIENTED_EDGE('',*,*,#5805,.T.);
#7874=ORIENTED_EDGE('',*,*,#5812,.F.);
#8252=CYLINDRICAL_SURFACE('',#10422,0.165);
#8253=CYLINDRICAL_SURFACE('',#10432,0.7);
#8254=CYLINDRICAL_SURFACE('',#10433,0.3);
#8255=CYLINDRICAL_SURFACE('',#10435,0.3);
#8732=ADVANCED_FACE('',(#1707),#8252,.F.);
#8733=ADVANCED_FACE('',(#1708),#1208,.T.);
#8734=ADVANCED_FACE('',(#1709,#945),#1209,.T.);
#8735=ADVANCED_FACE('',(#1710,#946),#1210,.F.);
#8736=ADVANCED_FACE('',(#1711),#8253,.T.);
#8737=ADVANCED_FACE('',(#1712),#8254,.T.);
#8738=ADVANCED_FACE('',(#1713),#8255,.T.);
#8739=ADVANCED_FACE('',(#1714,#947),#1211,.T.);
#8740=ADVANCED_FACE('',(#1715),#1212,.F.);
#8851=CLOSED_SHELL('',(#8732,#8733,#8734,#8735,#8736,#8737,#8738,#8739,
#8740));
#10421=AXIS2_PLACEMENT_3D('',#16212,#13054,#13055);
#10422=AXIS2_PLACEMENT_3D('',#16213,#13056,#13057);
#10423=AXIS2_PLACEMENT_3D('',#16215,#13058,#13059);
#10424=AXIS2_PLACEMENT_3D('',#16218,#13061,#13062);
#10425=AXIS2_PLACEMENT_3D('',#16219,#13063,#13064);
#10426=AXIS2_PLACEMENT_3D('',#16220,#13065,#13066);
#10427=AXIS2_PLACEMENT_3D('',#16222,#13067,#13068);
#10428=AXIS2_PLACEMENT_3D('',#16224,#13069,#13070);
#10429=AXIS2_PLACEMENT_3D('',#16225,#13071,#13072);
#10430=AXIS2_PLACEMENT_3D('',#16227,#13073,#13074);
#10431=AXIS2_PLACEMENT_3D('',#16229,#13075,#13076);
#10432=AXIS2_PLACEMENT_3D('',#16230,#13077,#13078);
#10433=AXIS2_PLACEMENT_3D('',#16232,#13080,#13081);
#10434=AXIS2_PLACEMENT_3D('',#16235,#13083,#13084);
#10435=AXIS2_PLACEMENT_3D('',#16236,#13085,#13086);
#10436=AXIS2_PLACEMENT_3D('',#16238,#13087,#13088);
#10437=AXIS2_PLACEMENT_3D('',#16240,#13090,#13091);
#10438=AXIS2_PLACEMENT_3D('',#16241,#13092,#13093);
#13054=DIRECTION('axis',(0.,0.,1.));
#13055=DIRECTION('refdir',(1.,0.,0.));
#13056=DIRECTION('center_axis',(0.,0.,1.));
#13057=DIRECTION('ref_axis',(1.,0.,0.));
#13058=DIRECTION('center_axis',(0.,0.,1.));
#13059=DIRECTION('ref_axis',(1.,0.,0.));
#13060=DIRECTION('',(0.,0.,1.));
#13061=DIRECTION('center_axis',(0.,0.,-1.));
#13062=DIRECTION('ref_axis',(1.,0.,0.));
#13063=DIRECTION('center_axis',(0.,0.,1.));
#13064=DIRECTION('ref_axis',(1.,0.,0.));
#13065=DIRECTION('center_axis',(0.,0.,1.));
#13066=DIRECTION('ref_axis',(1.,0.,0.));
#13067=DIRECTION('center_axis',(0.,0.,1.));
#13068=DIRECTION('ref_axis',(1.,0.,0.));
#13069=DIRECTION('center_axis',(0.,0.,1.));
#13070=DIRECTION('ref_axis',(1.,0.,0.));
#13071=DIRECTION('center_axis',(0.,0.,1.));
#13072=DIRECTION('ref_axis',(1.,0.,0.));
#13073=DIRECTION('center_axis',(0.,0.,1.));
#13074=DIRECTION('ref_axis',(1.,0.,0.));
#13075=DIRECTION('center_axis',(0.,0.,-1.));
#13076=DIRECTION('ref_axis',(1.,0.,0.));
#13077=DIRECTION('center_axis',(0.,0.,1.));
#13078=DIRECTION('ref_axis',(1.,0.,0.));
#13079=DIRECTION('',(0.,0.,-1.));
#13080=DIRECTION('center_axis',(0.,0.,1.));
#13081=DIRECTION('ref_axis',(1.,0.,0.));
#13082=DIRECTION('',(0.,0.,-1.));
#13083=DIRECTION('center_axis',(0.,0.,1.));
#13084=DIRECTION('ref_axis',(1.,0.,0.));
#13085=DIRECTION('center_axis',(0.,0.,1.));
#13086=DIRECTION('ref_axis',(1.,0.,0.));
#13087=DIRECTION('center_axis',(0.,0.,1.));
#13088=DIRECTION('ref_axis',(1.,0.,0.));
#13089=DIRECTION('',(0.,0.,-1.));
#13090=DIRECTION('center_axis',(0.,0.,1.));
#13091=DIRECTION('ref_axis',(1.,0.,0.));
#13092=DIRECTION('center_axis',(0.,0.,1.));
#13093=DIRECTION('ref_axis',(1.,0.,0.));
#16212=CARTESIAN_POINT('',(0.,0.,0.));
#16213=CARTESIAN_POINT('Origin',(4.,12.,7.1));
#16214=CARTESIAN_POINT('',(3.835,12.,7.1));
#16215=CARTESIAN_POINT('Origin',(4.,12.,7.1));
#16216=CARTESIAN_POINT('',(3.835,12.,8.1));
#16217=CARTESIAN_POINT('',(3.835,12.,7.1));
#16218=CARTESIAN_POINT('Origin',(4.,12.,8.1));
#16219=CARTESIAN_POINT('Origin',(4.,12.,7.1));
#16220=CARTESIAN_POINT('Origin',(4.,12.,6.1));
#16221=CARTESIAN_POINT('',(3.3,12.,6.1));
#16222=CARTESIAN_POINT('Origin',(4.,12.,6.1));
#16223=CARTESIAN_POINT('',(3.7,12.,6.1));
#16224=CARTESIAN_POINT('Origin',(4.,12.,6.1));
#16225=CARTESIAN_POINT('Origin',(4.,12.,5.7));
#16226=CARTESIAN_POINT('',(3.3,12.,5.7));
#16227=CARTESIAN_POINT('Origin',(4.,12.,5.7));
#16228=CARTESIAN_POINT('',(3.7,12.,5.7));
#16229=CARTESIAN_POINT('Origin',(4.,12.,5.7));
#16230=CARTESIAN_POINT('Origin',(4.,12.,5.7));
#16231=CARTESIAN_POINT('',(3.3,12.,5.7));
#16232=CARTESIAN_POINT('Origin',(4.,12.,5.2));
#16233=CARTESIAN_POINT('',(3.7,12.,5.2));
#16234=CARTESIAN_POINT('',(3.7,12.,5.2));
#16235=CARTESIAN_POINT('Origin',(4.,12.,5.2));
#16236=CARTESIAN_POINT('Origin',(4.,12.,5.2));
#16237=CARTESIAN_POINT('',(3.7,12.,8.1));
#16238=CARTESIAN_POINT('Origin',(4.,12.,8.1));
#16239=CARTESIAN_POINT('',(3.7,12.,5.2));
#16240=CARTESIAN_POINT('Origin',(4.,12.,8.1));
#16241=CARTESIAN_POINT('Origin',(4.,12.,5.2));
#16606=UNCERTAINTY_MEASURE_WITH_UNIT(LENGTH_MEASURE(0.001),#16679,
'DISTANCE_ACCURACY_VALUE',
'Maximum model space distance between geometric entities at asserted c
onnectivities');
#16614=UNCERTAINTY_MEASURE_WITH_UNIT(LENGTH_MEASURE(0.001),#16679,
'DISTANCE_ACCURACY_VALUE',
'Maximum model space distance between geometric entities at asserted c
onnectivities');
#16670=(
GEOMETRIC_REPRESENTATION_CONTEXT(3)
GLOBAL_UNCERTAINTY_ASSIGNED_CONTEXT((#16606))
GLOBAL_UNIT_ASSIGNED_CONTEXT((#16679,#16681,#16682))
REPRESENTATION_CONTEXT('','3D')
);
#16678=(
GEOMETRIC_REPRESENTATION_CONTEXT(3)
GLOBAL_UNCERTAINTY_ASSIGNED_CONTEXT((#16614))
GLOBAL_UNIT_ASSIGNED_CONTEXT((#16679,#16681,#16682))
REPRESENTATION_CONTEXT('','3D')
);
#16679=(
LENGTH_UNIT()
NAMED_UNIT(*)
SI_UNIT(.CENTI.,.METRE.)
);
#16681=(
NAMED_UNIT(*)
PLANE_ANGLE_UNIT()
SI_UNIT($,.RADIAN.)
);
#16682=(
NAMED_UNIT(*)
SI_UNIT($,.STERADIAN.)
SOLID_ANGLE_UNIT()
);
#16738=SHAPE_DEFINITION_REPRESENTATION(#16812,#16965);
#16812=PRODUCT_DEFINITION_SHAPE('',$,#17029);
#16965=SHAPE_REPRESENTATION('',(#10421),#16670);
#16973=PRODUCT_DEFINITION_CONTEXT('part definition',#17164,'design');
#17029=PRODUCT_DEFINITION('Vertical link pin (1)','Vertical link pin (1)',
#17092,#16973);
#17092=PRODUCT_DEFINITION_FORMATION('',$,#17221);
#17164=APPLICATION_CONTEXT(
'Core Data for Automotive Mechanical Design Process');
#17165=PRODUCT_CONTEXT('part definition',#17164,'mechanical');
#17221=PRODUCT('Vertical link pin (1)','Vertical link pin (1)',
'Vertical link pin (1)',(#17165));
#17285=COLOUR_RGB('Grey',0.48,0.52,0.57);
#17286=FILL_AREA_STYLE_COLOUR('',#17285);
#17287=FILL_AREA_STYLE('',(#17286));
#17288=SURFACE_STYLE_FILL_AREA(#17287);
#17289=SURFACE_SIDE_STYLE('',(#17288));
#17290=SURFACE_STYLE_USAGE(.BOTH.,#17289);
#17291=PRESENTATION_STYLE_ASSIGNMENT((#17290));
ENDSEC;
END-ISO-10303-21;
